ISO-10303-21;
HEADER;
/* Generated by software containing ST-Developer
 * from STEP Tools, Inc. (www.steptools.com) 
 */

FILE_DESCRIPTION(
/* description */ ('V-block with clamp strap'),
/* implementation_level */ '2;1');

FILE_NAME(
/* name */ 'Cap Screw - M5x20.step',
/* time_stamp */ '2026-10-27T10:50:53-07:00',
/* author */ (''),
/* organization */ (''),
/* preprocessor_version */ 'ST-DEVELOPER v20.2',
/* originating_system */ 'Autodesk Translation Framework v15.17.0.0',
/* authorisation */ '');

FILE_SCHEMA (('AUTOMOTIVE_DESIGN { 1 0 10303 214 3 1 1 }'));
ENDSEC;

DATA;
#10=MECHANICAL_DESIGN_GEOMETRIC_PRESENTATION_REPRESENTATION('',(#276),#7344);
#200=ORIENTED_CLOSED_SHELL('',*,#4160,.F.);
#206=CONICAL_SURFACE('',#4649,0.4,0.785398163397448);
#207=CONICAL_SURFACE('',#4653,0.41,0.785398163397448);
#208=CONICAL_SURFACE('',#4657,0.26,0.463647609000806);
#209=CONICAL_SURFACE('',#4661,0.225,0.785398163397448);
#218=BREP_WITH_VOIDS('Body1',#4159,(#200));
#234=SHAPE_REPRESENTATION_RELATIONSHIP('SRR','None',#7452,#255);
#255=ADVANCED_BREP_SHAPE_REPRESENTATION('',(#218),#7331);
#276=STYLED_ITEM('',(#7638),#218);
#356=FACE_BOUND('',#1006,.T.);
#454=CIRCLE('',#4648,0.375);
#455=CIRCLE('',#4650,0.425);
#456=CIRCLE('',#4652,0.425);
#457=CIRCLE('',#4654,0.395);
#458=CIRCLE('',#4656,0.27);
#459=CIRCLE('',#4658,0.24505);
#460=CIRCLE('',#4660,0.24505);
#461=CIRCLE('',#4662,0.2);
#542=CYLINDRICAL_SURFACE('',#4651,0.425);
#543=CYLINDRICAL_SURFACE('',#4659,0.24505);
#710=FACE_OUTER_BOUND('',#1001,.T.);
#711=FACE_OUTER_BOUND('',#1002,.T.);
#712=FACE_OUTER_BOUND('',#1003,.T.);
#713=FACE_OUTER_BOUND('',#1004,.T.);
#714=FACE_OUTER_BOUND('',#1005,.T.);
#715=FACE_OUTER_BOUND('',#1007,.T.);
#716=FACE_OUTER_BOUND('',#1008,.T.);
#717=FACE_OUTER_BOUND('',#1009,.T.);
#718=FACE_OUTER_BOUND('',#1010,.T.);
#719=FACE_OUTER_BOUND('',#1011,.T.);
#720=FACE_OUTER_BOUND('',#1012,.T.);
#721=FACE_OUTER_BOUND('',#1013,.T.);
#722=FACE_OUTER_BOUND('',#1014,.T.);
#723=FACE_OUTER_BOUND('',#1015,.T.);
#724=FACE_OUTER_BOUND('',#1016,.T.);
#725=FACE_OUTER_BOUND('',#1017,.T.);
#726=FACE_OUTER_BOUND('',#1018,.T.);
#1001=EDGE_LOOP('',(#3390));
#1002=EDGE_LOOP('',(#3391,#3392,#3393,#3394));
#1003=EDGE_LOOP('',(#3395,#3396,#3397,#3398));
#1004=EDGE_LOOP('',(#3399,#3400,#3401,#3402));
#1005=EDGE_LOOP('',(#3403));
#1006=EDGE_LOOP('',(#3404));
#1007=EDGE_LOOP('',(#3405,#3406,#3407,#3408));
#1008=EDGE_LOOP('',(#3409,#3410,#3411,#3412));
#1009=EDGE_LOOP('',(#3413,#3414,#3415,#3416));
#1010=EDGE_LOOP('',(#3417));
#1011=EDGE_LOOP('',(#3418,#3419,#3420,#3421));
#1012=EDGE_LOOP('',(#3422,#3423,#3424,#3425));
#1013=EDGE_LOOP('',(#3426,#3427,#3428,#3429));
#1014=EDGE_LOOP('',(#3430,#3431,#3432,#3433));
#1015=EDGE_LOOP('',(#3434,#3435,#3436,#3437));
#1016=EDGE_LOOP('',(#3438,#3439,#3440,#3441));
#1017=EDGE_LOOP('',(#3442,#3443,#3444,#3445,#3446,#3447));
#1018=EDGE_LOOP('',(#3448,#3449,#3450,#3451,#3452,#3453));
#1378=LINE('',#6818,#1743);
#1379=LINE('',#6822,#1744);
#1380=LINE('',#6826,#1745);
#1381=LINE('',#6833,#1746);
#1382=LINE('',#6837,#1747);
#1383=LINE('',#6841,#1748);
#1384=LINE('',#6846,#1749);
#1385=LINE('',#6848,#1750);
#1386=LINE('',#6850,#1751);
#1387=LINE('',#6851,#1752);
#1388=LINE('',#6854,#1753);
#1389=LINE('',#6856,#1754);
#1390=LINE('',#6857,#1755);
#1391=LINE('',#6860,#1756);
#1392=LINE('',#6862,#1757);
#1393=LINE('',#6863,#1758);
#1394=LINE('',#6866,#1759);
#1395=LINE('',#6868,#1760);
#1396=LINE('',#6869,#1761);
#1397=LINE('',#6872,#1762);
#1398=LINE('',#6874,#1763);
#1399=LINE('',#6875,#1764);
#1400=LINE('',#6877,#1765);
#1401=LINE('',#6878,#1766);
#1743=VECTOR('',#5602,0.4);
#1744=VECTOR('',#5607,0.425);
#1745=VECTOR('',#5612,0.41);
#1746=VECTOR('',#5621,0.26);
#1747=VECTOR('',#5626,0.25);
#1748=VECTOR('',#5631,0.225);
#1749=VECTOR('',#5636,1.);
#1750=VECTOR('',#5637,1.);
#1751=VECTOR('',#5638,1.);
#1752=VECTOR('',#5639,1.);
#1753=VECTOR('',#5642,1.);
#1754=VECTOR('',#5643,1.);
#1755=VECTOR('',#5644,1.);
#1756=VECTOR('',#5647,1.);
#1757=VECTOR('',#5648,1.);
#1758=VECTOR('',#5649,1.);
#1759=VECTOR('',#5652,1.);
#1760=VECTOR('',#5653,1.);
#1761=VECTOR('',#5654,1.);
#1762=VECTOR('',#5657,1.);
#1763=VECTOR('',#5658,1.);
#1764=VECTOR('',#5659,1.);
#1765=VECTOR('',#5662,1.);
#1766=VECTOR('',#5663,1.);
#2061=VERTEX_POINT('',#6813);
#2062=VERTEX_POINT('',#6816);
#2063=VERTEX_POINT('',#6820);
#2064=VERTEX_POINT('',#6824);
#2065=VERTEX_POINT('',#6828);
#2066=VERTEX_POINT('',#6831);
#2067=VERTEX_POINT('',#6835);
#2068=VERTEX_POINT('',#6839);
#2069=VERTEX_POINT('',#6844);
#2070=VERTEX_POINT('',#6845);
#2071=VERTEX_POINT('',#6847);
#2072=VERTEX_POINT('',#6849);
#2073=VERTEX_POINT('',#6853);
#2074=VERTEX_POINT('',#6855);
#2075=VERTEX_POINT('',#6859);
#2076=VERTEX_POINT('',#6861);
#2077=VERTEX_POINT('',#6865);
#2078=VERTEX_POINT('',#6867);
#2079=VERTEX_POINT('',#6871);
#2080=VERTEX_POINT('',#6873);
#2521=EDGE_CURVE('',#2061,#2061,#454,.T.);
#2522=EDGE_CURVE('',#2062,#2062,#455,.T.);
#2523=EDGE_CURVE('',#2062,#2061,#1378,.T.);
#2524=EDGE_CURVE('',#2063,#2063,#456,.T.);
#2525=EDGE_CURVE('',#2063,#2062,#1379,.T.);
#2526=EDGE_CURVE('',#2064,#2064,#457,.T.);
#2527=EDGE_CURVE('',#2064,#2063,#1380,.T.);
#2528=EDGE_CURVE('',#2065,#2065,#458,.T.);
#2529=EDGE_CURVE('',#2066,#2066,#459,.F.);
#2530=EDGE_CURVE('',#2066,#2065,#1381,.T.);
#2531=EDGE_CURVE('',#2067,#2067,#460,.F.);
#2532=EDGE_CURVE('',#2067,#2066,#1382,.T.);
#2533=EDGE_CURVE('',#2068,#2068,#461,.T.);
#2534=EDGE_CURVE('',#2068,#2067,#1383,.T.);
#2535=EDGE_CURVE('',#2069,#2070,#1384,.T.);
#2536=EDGE_CURVE('',#2070,#2071,#1385,.T.);
#2537=EDGE_CURVE('',#2071,#2072,#1386,.T.);
#2538=EDGE_CURVE('',#2069,#2072,#1387,.T.);
#2539=EDGE_CURVE('',#2070,#2073,#1388,.T.);
#2540=EDGE_CURVE('',#2073,#2074,#1389,.T.);
#2541=EDGE_CURVE('',#2074,#2071,#1390,.T.);
#2542=EDGE_CURVE('',#2073,#2075,#1391,.T.);
#2543=EDGE_CURVE('',#2075,#2076,#1392,.T.);
#2544=EDGE_CURVE('',#2076,#2074,#1393,.T.);
#2545=EDGE_CURVE('',#2075,#2077,#1394,.T.);
#2546=EDGE_CURVE('',#2077,#2078,#1395,.T.);
#2547=EDGE_CURVE('',#2078,#2076,#1396,.T.);
#2548=EDGE_CURVE('',#2077,#2079,#1397,.T.);
#2549=EDGE_CURVE('',#2079,#2080,#1398,.T.);
#2550=EDGE_CURVE('',#2080,#2078,#1399,.T.);
#2551=EDGE_CURVE('',#2079,#2069,#1400,.T.);
#2552=EDGE_CURVE('',#2072,#2080,#1401,.T.);
#3390=ORIENTED_EDGE('',*,*,#2521,.F.);
#3391=ORIENTED_EDGE('',*,*,#2522,.F.);
#3392=ORIENTED_EDGE('',*,*,#2523,.T.);
#3393=ORIENTED_EDGE('',*,*,#2521,.T.);
#3394=ORIENTED_EDGE('',*,*,#2523,.F.);
#3395=ORIENTED_EDGE('',*,*,#2524,.F.);
#3396=ORIENTED_EDGE('',*,*,#2525,.T.);
#3397=ORIENTED_EDGE('',*,*,#2522,.T.);
#3398=ORIENTED_EDGE('',*,*,#2525,.F.);
#3399=ORIENTED_EDGE('',*,*,#2526,.F.);
#3400=ORIENTED_EDGE('',*,*,#2527,.T.);
#3401=ORIENTED_EDGE('',*,*,#2524,.T.);
#3402=ORIENTED_EDGE('',*,*,#2527,.F.);
#3403=ORIENTED_EDGE('',*,*,#2526,.T.);
#3404=ORIENTED_EDGE('',*,*,#2528,.F.);
#3405=ORIENTED_EDGE('',*,*,#2529,.F.);
#3406=ORIENTED_EDGE('',*,*,#2530,.T.);
#3407=ORIENTED_EDGE('',*,*,#2528,.T.);
#3408=ORIENTED_EDGE('',*,*,#2530,.F.);
#3409=ORIENTED_EDGE('',*,*,#2531,.F.);
#3410=ORIENTED_EDGE('',*,*,#2532,.T.);
#3411=ORIENTED_EDGE('',*,*,#2529,.T.);
#3412=ORIENTED_EDGE('',*,*,#2532,.F.);
#3413=ORIENTED_EDGE('',*,*,#2533,.F.);
#3414=ORIENTED_EDGE('',*,*,#2534,.T.);
#3415=ORIENTED_EDGE('',*,*,#2531,.T.);
#3416=ORIENTED_EDGE('',*,*,#2534,.F.);
#3417=ORIENTED_EDGE('',*,*,#2533,.T.);
#3418=ORIENTED_EDGE('',*,*,#2535,.T.);
#3419=ORIENTED_EDGE('',*,*,#2536,.T.);
#3420=ORIENTED_EDGE('',*,*,#2537,.T.);
#3421=ORIENTED_EDGE('',*,*,#2538,.F.);
#3422=ORIENTED_EDGE('',*,*,#2539,.T.);
#3423=ORIENTED_EDGE('',*,*,#2540,.T.);
#3424=ORIENTED_EDGE('',*,*,#2541,.T.);
#3425=ORIENTED_EDGE('',*,*,#2536,.F.);
#3426=ORIENTED_EDGE('',*,*,#2542,.T.);
#3427=ORIENTED_EDGE('',*,*,#2543,.T.);
#3428=ORIENTED_EDGE('',*,*,#2544,.T.);
#3429=ORIENTED_EDGE('',*,*,#2540,.F.);
#3430=ORIENTED_EDGE('',*,*,#2545,.T.);
#3431=ORIENTED_EDGE('',*,*,#2546,.T.);
#3432=ORIENTED_EDGE('',*,*,#2547,.T.);
#3433=ORIENTED_EDGE('',*,*,#2543,.F.);
#3434=ORIENTED_EDGE('',*,*,#2548,.T.);
#3435=ORIENTED_EDGE('',*,*,#2549,.T.);
#3436=ORIENTED_EDGE('',*,*,#2550,.T.);
#3437=ORIENTED_EDGE('',*,*,#2546,.F.);
#3438=ORIENTED_EDGE('',*,*,#2551,.T.);
#3439=ORIENTED_EDGE('',*,*,#2538,.T.);
#3440=ORIENTED_EDGE('',*,*,#2552,.T.);
#3441=ORIENTED_EDGE('',*,*,#2549,.F.);
#3442=ORIENTED_EDGE('',*,*,#2551,.F.);
#3443=ORIENTED_EDGE('',*,*,#2548,.F.);
#3444=ORIENTED_EDGE('',*,*,#2545,.F.);
#3445=ORIENTED_EDGE('',*,*,#2542,.F.);
#3446=ORIENTED_EDGE('',*,*,#2539,.F.);
#3447=ORIENTED_EDGE('',*,*,#2535,.F.);
#3448=ORIENTED_EDGE('',*,*,#2552,.F.);
#3449=ORIENTED_EDGE('',*,*,#2537,.F.);
#3450=ORIENTED_EDGE('',*,*,#2541,.F.);
#3451=ORIENTED_EDGE('',*,*,#2544,.F.);
#3452=ORIENTED_EDGE('',*,*,#2547,.F.);
#3453=ORIENTED_EDGE('',*,*,#2550,.F.);
#3847=PLANE('',#4647);
#3848=PLANE('',#4655);
#3849=PLANE('',#4663);
#3850=PLANE('',#4664);
#3851=PLANE('',#4665);
#3852=PLANE('',#4666);
#3853=PLANE('',#4667);
#3854=PLANE('',#4668);
#3855=PLANE('',#4669);
#3856=PLANE('',#4670);
#3857=PLANE('',#4671);
#4056=ADVANCED_FACE('',(#710),#3847,.T.);
#4057=ADVANCED_FACE('',(#711),#206,.T.);
#4058=ADVANCED_FACE('',(#712),#542,.T.);
#4059=ADVANCED_FACE('',(#713),#207,.T.);
#4060=ADVANCED_FACE('',(#714,#356),#3848,.T.);
#4061=ADVANCED_FACE('',(#715),#208,.T.);
#4062=ADVANCED_FACE('',(#716),#543,.T.);
#4063=ADVANCED_FACE('',(#717),#209,.T.);
#4064=ADVANCED_FACE('',(#718),#3849,.T.);
#4065=ADVANCED_FACE('',(#719),#3850,.F.);
#4066=ADVANCED_FACE('',(#720),#3851,.F.);
#4067=ADVANCED_FACE('',(#721),#3852,.F.);
#4068=ADVANCED_FACE('',(#722),#3853,.F.);
#4069=ADVANCED_FACE('',(#723),#3854,.F.);
#4070=ADVANCED_FACE('',(#724),#3855,.F.);
#4071=ADVANCED_FACE('',(#725),#3856,.F.);
#4072=ADVANCED_FACE('',(#726),#3857,.F.);
#4159=CLOSED_SHELL('',(#4056,#4057,#4058,#4059,#4060,#4061,#4062,#4063,
#4064));
#4160=CLOSED_SHELL('',(#4065,#4066,#4067,#4068,#4069,#4070,#4071,#4072));
#4646=AXIS2_PLACEMENT_3D('',#6811,#5592,#5593);
#4647=AXIS2_PLACEMENT_3D('',#6812,#5594,#5595);
#4648=AXIS2_PLACEMENT_3D('',#6814,#5596,#5597);
#4649=AXIS2_PLACEMENT_3D('',#6815,#5598,#5599);
#4650=AXIS2_PLACEMENT_3D('',#6817,#5600,#5601);
#4651=AXIS2_PLACEMENT_3D('',#6819,#5603,#5604);
#4652=AXIS2_PLACEMENT_3D('',#6821,#5605,#5606);
#4653=AXIS2_PLACEMENT_3D('',#6823,#5608,#5609);
#4654=AXIS2_PLACEMENT_3D('',#6825,#5610,#5611);
#4655=AXIS2_PLACEMENT_3D('',#6827,#5613,#5614);
#4656=AXIS2_PLACEMENT_3D('',#6829,#5615,#5616);
#4657=AXIS2_PLACEMENT_3D('',#6830,#5617,#5618);
#4658=AXIS2_PLACEMENT_3D('',#6832,#5619,#5620);
#4659=AXIS2_PLACEMENT_3D('',#6834,#5622,#5623);
#4660=AXIS2_PLACEMENT_3D('',#6836,#5624,#5625);
#4661=AXIS2_PLACEMENT_3D('',#6838,#5627,#5628);
#4662=AXIS2_PLACEMENT_3D('',#6840,#5629,#5630);
#4663=AXIS2_PLACEMENT_3D('',#6842,#5632,#5633);
#4664=AXIS2_PLACEMENT_3D('',#6843,#5634,#5635);
#4665=AXIS2_PLACEMENT_3D('',#6852,#5640,#5641);
#4666=AXIS2_PLACEMENT_3D('',#6858,#5645,#5646);
#4667=AXIS2_PLACEMENT_3D('',#6864,#5650,#5651);
#4668=AXIS2_PLACEMENT_3D('',#6870,#5655,#5656);
#4669=AXIS2_PLACEMENT_3D('',#6876,#5660,#5661);
#4670=AXIS2_PLACEMENT_3D('',#6879,#5664,#5665);
#4671=AXIS2_PLACEMENT_3D('',#6880,#5666,#5667);
#5592=DIRECTION('axis',(0.,0.,1.));
#5593=DIRECTION('refdir',(1.,0.,0.));
#5594=DIRECTION('center_axis',(0.,1.,0.));
#5595=DIRECTION('ref_axis',(0.,0.,1.));
#5596=DIRECTION('center_axis',(0.,-1.,0.));
#5597=DIRECTION('ref_axis',(1.,0.,0.));
#5598=DIRECTION('center_axis',(0.,-1.,0.));
#5599=DIRECTION('ref_axis',(1.,0.,0.));
#5600=DIRECTION('center_axis',(0.,-1.,0.));
#5601=DIRECTION('ref_axis',(1.,0.,0.));
#5602=DIRECTION('',(0.707106781186548,0.707106781186547,8.65956056235493E-17));
#5603=DIRECTION('center_axis',(0.,-1.,0.));
#5604=DIRECTION('ref_axis',(1.,0.,0.));
#5605=DIRECTION('center_axis',(0.,-1.,0.));
#5606=DIRECTION('ref_axis',(1.,0.,0.));
#5607=DIRECTION('',(0.,1.,0.));
#5608=DIRECTION('center_axis',(0.,1.,0.));
#5609=DIRECTION('ref_axis',(1.,0.,0.));
#5610=DIRECTION('center_axis',(0.,-1.,0.));
#5611=DIRECTION('ref_axis',(1.,0.,0.));
#5612=DIRECTION('',(-0.707106781186547,0.707106781186548,-8.65956056235493E-17));
#5613=DIRECTION('center_axis',(0.,-1.,0.));
#5614=DIRECTION('ref_axis',(0.,0.,-1.));
#5615=DIRECTION('center_axis',(0.,-1.,0.));
#5616=DIRECTION('ref_axis',(1.,0.,0.));
#5617=DIRECTION('center_axis',(0.,1.,0.));
#5618=DIRECTION('ref_axis',(1.,0.,0.));
#5619=DIRECTION('center_axis',(0.,1.,0.));
#5620=DIRECTION('ref_axis',(1.,0.,0.));
#5621=DIRECTION('',(-0.447213595499958,0.894427190999916,-5.47678698264203E-17));
#5622=DIRECTION('center_axis',(0.,-1.,0.));
#5623=DIRECTION('ref_axis',(1.,0.,0.));
#5624=DIRECTION('center_axis',(0.,1.,0.));
#5625=DIRECTION('ref_axis',(1.,0.,0.));
#5626=DIRECTION('',(0.,1.,0.));
#5627=DIRECTION('center_axis',(0.,1.,0.));
#5628=DIRECTION('ref_axis',(1.,0.,0.));
#5629=DIRECTION('center_axis',(0.,-1.,0.));
#5630=DIRECTION('ref_axis',(1.,0.,0.));
#5631=DIRECTION('',(-0.707106781186547,0.707106781186548,-8.65956056235493E-17));
#5632=DIRECTION('center_axis',(0.,-1.,0.));
#5633=DIRECTION('ref_axis',(0.,0.,-1.));
#5634=DIRECTION('center_axis',(0.866025403784439,0.,-0.5));
#5635=DIRECTION('ref_axis',(0.5,0.,0.866025403784439));
#5636=DIRECTION('',(-0.5,0.,-0.866025403784439));
#5637=DIRECTION('',(0.,-1.,0.));
#5638=DIRECTION('',(0.5,0.,0.866025403784439));
#5639=DIRECTION('',(0.,-1.,0.));
#5640=DIRECTION('center_axis',(1.20185167898973E-16,0.,-1.));
#5641=DIRECTION('ref_axis',(1.,0.,1.20185167898973E-16));
#5642=DIRECTION('',(-1.,0.,-1.20185167898973E-16));
#5643=DIRECTION('',(0.,-1.,0.));
#5644=DIRECTION('',(1.,0.,1.20185167898973E-16));
#5645=DIRECTION('center_axis',(-0.866025403784439,0.,-0.5));
#5646=DIRECTION('ref_axis',(0.5,0.,-0.866025403784439));
#5647=DIRECTION('',(-0.5,0.,0.866025403784439));
#5648=DIRECTION('',(0.,-1.,0.));
#5649=DIRECTION('',(0.5,0.,-0.866025403784439));
#5650=DIRECTION('center_axis',(-0.866025403784439,0.,0.5));
#5651=DIRECTION('ref_axis',(-0.5,0.,-0.866025403784439));
#5652=DIRECTION('',(0.5,0.,0.866025403784439));
#5653=DIRECTION('',(0.,-1.,0.));
#5654=DIRECTION('',(-0.5,0.,-0.866025403784439));
#5655=DIRECTION('center_axis',(-2.40370335797945E-16,0.,1.));
#5656=DIRECTION('ref_axis',(-1.,0.,-2.40370335797945E-16));
#5657=DIRECTION('',(1.,0.,2.40370335797945E-16));
#5658=DIRECTION('',(0.,-1.,0.));
#5659=DIRECTION('',(-1.,0.,-2.40370335797945E-16));
#5660=DIRECTION('center_axis',(0.866025403784439,0.,0.5));
#5661=DIRECTION('ref_axis',(-0.5,0.,0.866025403784439));
#5662=DIRECTION('',(0.5,0.,-0.866025403784439));
#5663=DIRECTION('',(-0.5,0.,0.866025403784439));
#5664=DIRECTION('center_axis',(0.,1.,0.));
#5665=DIRECTION('ref_axis',(1.,0.,0.));
#5666=DIRECTION('center_axis',(0.,-1.,0.));
#5667=DIRECTION('ref_axis',(0.,0.,-1.));
#6811=CARTESIAN_POINT('',(0.,0.,0.));
#6812=CARTESIAN_POINT('Origin',(0.375,0.5,0.));
#6813=CARTESIAN_POINT('',(-0.375,0.5,-4.59242549680257E-17));
#6814=CARTESIAN_POINT('Origin',(0.,0.5,0.));
#6815=CARTESIAN_POINT('Origin',(0.,0.475,0.));
#6816=CARTESIAN_POINT('',(-0.425,0.45,-5.20474889637625E-17));
#6817=CARTESIAN_POINT('Origin',(0.,0.45,0.));
#6818=CARTESIAN_POINT('',(-0.4,0.475,-4.89858719658941E-17));
#6819=CARTESIAN_POINT('Origin',(0.,0.24,0.));
#6820=CARTESIAN_POINT('',(-0.425,0.0299999999999998,-5.20474889637625E-17));
#6821=CARTESIAN_POINT('Origin',(0.,0.0299999999999998,0.));
#6822=CARTESIAN_POINT('',(-0.425,0.24,-5.20474889637625E-17));
#6823=CARTESIAN_POINT('Origin',(0.,0.0150000000000001,0.));
#6824=CARTESIAN_POINT('',(-0.395,4.85722573273506E-17,-4.83735485663204E-17));
#6825=CARTESIAN_POINT('Origin',(0.,0.,0.));
#6826=CARTESIAN_POINT('',(-0.41,0.0150000000000001,-5.02105187650415E-17));
#6827=CARTESIAN_POINT('Origin',(0.27,0.,0.));
#6828=CARTESIAN_POINT('',(-0.27,0.,-3.30654635769785E-17));
#6829=CARTESIAN_POINT('Origin',(0.,0.,0.));
#6830=CARTESIAN_POINT('Origin',(0.,-0.02,0.));
#6831=CARTESIAN_POINT('',(-0.24505,-0.0498999999999999,3.00099698131059E-17));
#6832=CARTESIAN_POINT('Origin',(0.,-0.0498999999999999,0.));
#6833=CARTESIAN_POINT('',(-0.26,-0.02,-3.18408167778312E-17));
#6834=CARTESIAN_POINT('Origin',(0.,-0.995,0.));
#6835=CARTESIAN_POINT('',(-0.24505,-1.95495,3.00099698131059E-17));
#6836=CARTESIAN_POINT('Origin',(0.,-1.95495,0.));
#6837=CARTESIAN_POINT('',(-0.24505,-0.995,-3.00099698131059E-17));
#6838=CARTESIAN_POINT('Origin',(0.,-1.975,0.));
#6839=CARTESIAN_POINT('',(-0.2,-2.,-2.44929359829471E-17));
#6840=CARTESIAN_POINT('Origin',(0.,-2.,0.));
#6841=CARTESIAN_POINT('',(-0.225,-1.975,-2.75545529808154E-17));
#6842=CARTESIAN_POINT('Origin',(0.,-2.,0.));
#6843=CARTESIAN_POINT('Origin',(0.115470053837925,-0.5,-0.2));
#6844=CARTESIAN_POINT('',(0.23094010767585,-0.5,0.));
#6845=CARTESIAN_POINT('',(0.115470053837925,-0.5,-0.2));
#6846=CARTESIAN_POINT('',(0.23094010767585,-0.5,0.));
#6847=CARTESIAN_POINT('',(0.115470053837925,-0.8,-0.2));
#6848=CARTESIAN_POINT('',(0.115470053837925,-0.5,-0.2));
#6849=CARTESIAN_POINT('',(0.23094010767585,-0.8,0.));
#6850=CARTESIAN_POINT('',(0.23094010767585,-0.8,0.));
#6851=CARTESIAN_POINT('',(0.23094010767585,-0.5,0.));
#6852=CARTESIAN_POINT('Origin',(-0.115470053837925,-0.5,-0.2));
#6853=CARTESIAN_POINT('',(-0.115470053837925,-0.5,-0.2));
#6854=CARTESIAN_POINT('',(0.115470053837925,-0.5,-0.2));
#6855=CARTESIAN_POINT('',(-0.115470053837925,-0.8,-0.2));
#6856=CARTESIAN_POINT('',(-0.115470053837925,-0.5,-0.2));
#6857=CARTESIAN_POINT('',(0.115470053837925,-0.8,-0.2));
#6858=CARTESIAN_POINT('Origin',(-0.23094010767585,-0.5,-2.77555756156289E-17));
#6859=CARTESIAN_POINT('',(-0.23094010767585,-0.5,-2.82820063659975E-17));
#6860=CARTESIAN_POINT('',(-0.115470053837925,-0.5,-0.2));
#6861=CARTESIAN_POINT('',(-0.23094010767585,-0.8,-2.77555756156289E-17));
#6862=CARTESIAN_POINT('',(-0.23094010767585,-0.5,-2.82820063659975E-17));
#6863=CARTESIAN_POINT('',(-0.115470053837925,-0.8,-0.2));
#6864=CARTESIAN_POINT('Origin',(-0.115470053837925,-0.5,0.2));
#6865=CARTESIAN_POINT('',(-0.115470053837925,-0.5,0.2));
#6866=CARTESIAN_POINT('',(-0.23094010767585,-0.5,-2.82820063659975E-17));
#6867=CARTESIAN_POINT('',(-0.115470053837925,-0.8,0.2));
#6868=CARTESIAN_POINT('',(-0.115470053837925,-0.5,0.2));
#6869=CARTESIAN_POINT('',(-0.23094010767585,-0.8,-2.82820063659975E-17));
#6870=CARTESIAN_POINT('Origin',(0.115470053837925,-0.5,0.2));
#6871=CARTESIAN_POINT('',(0.115470053837925,-0.5,0.2));
#6872=CARTESIAN_POINT('',(-0.115470053837925,-0.5,0.2));
#6873=CARTESIAN_POINT('',(0.115470053837925,-0.8,0.2));
#6874=CARTESIAN_POINT('',(0.115470053837925,-0.5,0.2));
#6875=CARTESIAN_POINT('',(-0.115470053837925,-0.8,0.2));
#6876=CARTESIAN_POINT('Origin',(0.23094010767585,-0.5,0.));
#6877=CARTESIAN_POINT('',(0.115470053837925,-0.5,0.2));
#6878=CARTESIAN_POINT('',(0.115470053837925,-0.8,0.2));
#6879=CARTESIAN_POINT('Origin',(0.,-0.5,0.));
#6880=CARTESIAN_POINT('Origin',(0.,-0.8,0.));
#7305=UNCERTAINTY_MEASURE_WITH_UNIT(LENGTH_MEASURE(0.001),#7345,
'DISTANCE_ACCURACY_VALUE',
'Maximum model space distance between geometric entities at asserted c
onnectivities');
#7318=UNCERTAINTY_MEASURE_WITH_UNIT(LENGTH_MEASURE(0.001),#7345,
'DISTANCE_ACCURACY_VALUE',
'Maximum model space distance between geometric entities at asserted c
onnectivities');
#7331=(
GEOMETRIC_REPRESENTATION_CONTEXT(3)
GLOBAL_UNCERTAINTY_ASSIGNED_CONTEXT((#7305))
GLOBAL_UNIT_ASSIGNED_CONTEXT((#7345,#7347,#7348))
REPRESENTATION_CONTEXT('','3D')
);
#7344=(
GEOMETRIC_REPRESENTATION_CONTEXT(3)
GLOBAL_UNCERTAINTY_ASSIGNED_CONTEXT((#7318))
GLOBAL_UNIT_ASSIGNED_CONTEXT((#7345,#7347,#7348))
REPRESENTATION_CONTEXT('','3D')
);
#7345=(
LENGTH_UNIT()
NAMED_UNIT(*)
SI_UNIT(.CENTI.,.METRE.)
);
#7347=(
NAMED_UNIT(*)
PLANE_ANGLE_UNIT()
SI_UNIT($,.RADIAN.)
);
#7348=(
NAMED_UNIT(*)
SI_UNIT($,.STERADIAN.)
SOLID_ANGLE_UNIT()
);
#7361=SHAPE_DEFINITION_REPRESENTATION(#7386,#7452);
#7386=PRODUCT_DEFINITION_SHAPE('',$,#7478);
#7452=SHAPE_REPRESENTATION('',(#4646),#7331);
#7465=PRODUCT_DEFINITION_CONTEXT('part definition',#7542,'design');
#7478=PRODUCT_DEFINITION('Cap Screw - M5x20','Cap Screw - M5x20',#7503,
#7465);
#7503=PRODUCT_DEFINITION_FORMATION('',$,#7556);
#7542=APPLICATION_CONTEXT(
'Core Data for Automotive Mechanical Design Process');
#7543=PRODUCT_CONTEXT('part definition',#7542,'mechanical');
#7556=PRODUCT('Cap Screw - M5x20','Cap Screw - M5x20',
'Cap Screw - M5x20',(#7543));
#7632=COLOUR_RGB('Black',0.12,0.14,0.17);
#7633=FILL_AREA_STYLE_COLOUR('',#7632);
#7634=FILL_AREA_STYLE('',(#7633));
#7635=SURFACE_STYLE_FILL_AREA(#7634);
#7636=SURFACE_SIDE_STYLE('',(#7635));
#7637=SURFACE_STYLE_USAGE(.BOTH.,#7636);
#7638=PRESENTATION_STYLE_ASSIGNMENT((#7637));
ENDSEC;
END-ISO-10303-21;
